ISO-10303-21;
HEADER;
FILE_DESCRIPTION (('STEP AP214'),
    '1' );
FILE_NAME ('Rod.step',
    '2026-10-06T08:09:25',
    ( '' ),
    ( '' ),
    'SwSTEP 2.0',
    'SolidWorks 2021',
    '' );
FILE_SCHEMA (( 'AUTOMOTIVE_DESIGN' ));
ENDSEC;

DATA;
#81=EDGE_CURVE ( 'NONE', #17539, #20156, #20469, .T. ) ;
#159=SURFACE_STYLE_FILL_AREA ( #10728 ) ;
#235=VERTEX_POINT ( 'NONE', #17541 ) ;
#378=ORIENTED_EDGE ( 'NONE', *, *, #16785, .T. ) ;
#380=LINE ( 'NONE', #5677, #10534 ) ;
#466=DIRECTION ( 'NONE',  ( 5.551115123125797493E-17, -2.869019762633797485E-16, -1.000000000000000000 ) ) ;
#492=ADVANCED_FACE ( 'NONE', ( #12334 ), #15856, .T. ) ;
#495=SURFACE_SIDE_STYLE ('',( #16812 ) ) ;
#581=CARTESIAN_POINT ( 'NONE',  ( -3.097832296507313600E-14, 60.00000000000000000, -4.249999999999968914 ) ) ;
#629=UNCERTAINTY_MEASURE_WITH_UNIT (LENGTH_MEASURE( 1.000000000000000082E-05 ), #16359, 'distance_accuracy_value', 'NONE');
#803=AXIS2_PLACEMENT_3D ( 'NONE', #4880, #13195, #16816 ) ;
#808=ORIENTED_EDGE ( 'NONE', *, *, #21708, .T. ) ;
#838=PRODUCT ( 'Rod', 'Rod', '', ( #5665 ) ) ;
#913=EDGE_CURVE ( 'NONE', #7934, #15346, #11036, .T. ) ;
#928=AXIS2_PLACEMENT_3D ( 'NONE', #22168, #18404, #9464 ) ;
#970=COLOUR_RGB ( '', 0.40784314, 0.44705882, 0.49803922) ;
#1132=PRODUCT_DEFINITION_FORMATION_WITH_SPECIFIED_SOURCE ( 'ANY', '', #838, .NOT_KNOWN. ) ;
#1222=CARTESIAN_POINT ( 'NONE',  ( -3.122502256758252770E-14, 59.74999999999991473, 2.081668171172168513E-14 ) ) ;
#1324=ADVANCED_BREP_SHAPE_REPRESENTATION ( '', ( #5581, #22115 ), #19511 ) ;
#1410=SURFACE_STYLE_USAGE ( .BOTH. , #17513 ) ;
#1426=CIRCLE ( 'NONE', #20211, 2.499999999999993783 ) ;
#1465=CARTESIAN_POINT ( 'NONE',  ( 2.773872027545001791E-14, 1.041826426137094221E-16, 2.500000000000000000 ) ) ;
#1480=DIRECTION ( 'NONE',  ( -3.070652698126927723E-17, -1.000000000000000000, 4.167305704548413124E-17 ) ) ;
#1484=DIRECTION ( 'NONE',  ( -5.551115123125796261E-17, 0.000000000000000000, 1.000000000000000000 ) ) ;
#1497=EDGE_LOOP ( 'NONE', ( #20808, #7884, #3817, #2556 ) ) ;
#1550=VERTEX_POINT ( 'NONE', #10840 ) ;
#1558=CYLINDRICAL_SURFACE ( 'NONE', #19515, 2.499999999999993783 ) ;
#1560=DIRECTION ( 'NONE',  ( 5.551115123125733398E-17, 0.000000000000000000, -1.000000000000000000 ) ) ;
#1712=SURFACE_STYLE_USAGE ( .BOTH. , #19589 ) ;
#1895=FACE_OUTER_BOUND ( 'NONE', #18949, .T. ) ;
#2001=PRODUCT_DEFINITION ( 'UNKNOWN', '', #1132, #10993 ) ;
#2084=PLANE ( 'NONE',  #14547 ) ;
#2109=EDGE_CURVE ( 'NONE', #12680, #1550, #1426, .T. ) ;
#2497=ORIENTED_EDGE ( 'NONE', *, *, #13892, .T. ) ;
#2555=ORIENTED_EDGE ( 'NONE', *, *, #17567, .F. ) ;
#2556=ORIENTED_EDGE ( 'NONE', *, *, #20753, .F. ) ;
#2599=SURFACE_SIDE_STYLE ('',( #18380 ) ) ;
#2849=ORIENTED_EDGE ( 'NONE', *, *, #7969, .F. ) ;
#2963=DIRECTION ( 'NONE',  ( 0.000000000000000000, 0.000000000000000000, 1.000000000000000000 ) ) ;
#3255=PRESENTATION_STYLE_ASSIGNMENT (( #1712 ) ) ;
#3301=EDGE_CURVE ( 'NONE', #7035, #10831, #20204, .T. ) ;
#3394=CARTESIAN_POINT ( 'NONE',  ( 0.000000000000000000, 0.000000000000000000, 0.000000000000000000 ) ) ;
#3532=PRESENTATION_STYLE_ASSIGNMENT (( #1410 ) ) ;
#3576=SURFACE_STYLE_FILL_AREA ( #19693 ) ;
#3663=ORIENTED_EDGE ( 'NONE', *, *, #4894, .F. ) ;
#3669=ADVANCED_FACE ( 'NONE', ( #9731 ), #5739, .T. ) ;
#3706=DIRECTION ( 'NONE',  ( -3.070652698126927723E-17, -1.000000000000000000, 4.167305704548413124E-17 ) ) ;
#3775=DIRECTION ( 'NONE',  ( -3.070652698126927723E-17, -1.000000000000000000, 4.167305704548413124E-17 ) ) ;
#3777=PRESENTATION_STYLE_ASSIGNMENT (( #7328 ) ) ;
#3817=ORIENTED_EDGE ( 'NONE', *, *, #20792, .T. ) ;
#3839=VECTOR ( 'NONE', #11903, 1000.000000000000000 ) ;
#3897=DIRECTION ( 'NONE',  ( -3.070652698126927723E-17, -1.000000000000000000, 4.167305704548413124E-17 ) ) ;
#3911=ORIENTED_EDGE ( 'NONE', *, *, #14153, .F. ) ;
#3975=DIRECTION ( 'NONE',  ( 2.563050070131097656E-17, -0.7071067811865543451, 0.7071067811865406894 ) ) ;
#4044=FACE_OUTER_BOUND ( 'NONE', #1497, .T. ) ;
#4100=( GEOMETRIC_REPRESENTATION_CONTEXT ( 3 ) GLOBAL_UNCERTAINTY_ASSIGNED_CONTEXT ( ( #6296 ) ) GLOBAL_UNIT_ASSIGNED_CONTEXT ( ( #21237, #19567, #20036 ) ) REPRESENTATION_CONTEXT ( 'NONE', 'WORKASPACE' ) );
#4120=CARTESIAN_POINT ( 'NONE',  ( -3.122502256758252770E-14, 59.74999999999991473, 2.081668171172168513E-14 ) ) ;
#4185=DIRECTION ( 'NONE',  ( 5.551115123125796261E-17, -2.869019762633796499E-16, -1.000000000000000000 ) ) ;
#4214=MECHANICAL_DESIGN_GEOMETRIC_PRESENTATION_REPRESENTATION('',(#17365),#16986);
#4302=STYLED_ITEM ( 'NONE', ( #22247 ), #19798 ) ;
#4348=( NAMED_UNIT ( * ) PLANE_ANGLE_UNIT ( ) SI_UNIT ( $, .RADIAN. ) );
#4550=( GEOMETRIC_REPRESENTATION_CONTEXT ( 3 ) GLOBAL_UNCERTAINTY_ASSIGNED_CONTEXT ( ( #8145 ) ) GLOBAL_UNIT_ASSIGNED_CONTEXT ( ( #10644, #8890, #14301 ) ) REPRESENTATION_CONTEXT ( 'NONE', 'WORKASPACE' ) );
#4672=CLOSED_SHELL ( 'NONE', ( #11669, #7961, #492, #3669, #19798, #15997, #20730, #22456, #17874 ) ) ;
#4738=VECTOR ( 'NONE', #3975, 1000.000000000000227 ) ;
#4789=AXIS2_PLACEMENT_3D ( 'NONE', #11624, #16556, #466 ) ;
#4880=CARTESIAN_POINT ( 'NONE',  ( -3.122502256758252770E-14, 59.74999999999991473, 2.081668171172168513E-14 ) ) ;
#4894=EDGE_CURVE ( 'NONE', #10831, #7035, #12625, .T. ) ;
#4943=CARTESIAN_POINT ( 'NONE',  ( 0.000000000000000000, 0.000000000000000000, 0.000000000000000000 ) ) ;
#4962=LINE ( 'NONE', #18982, #3839 ) ;
#5044=EDGE_CURVE ( 'NONE', #7934, #10595, #8130, .T. ) ;
#5057=FILL_AREA_STYLE ('',( #6593 ) ) ;
#5172=( LENGTH_UNIT ( ) NAMED_UNIT ( * ) SI_UNIT ( .MILLI., .METRE. ) );
#5214=( LENGTH_UNIT ( ) NAMED_UNIT ( * ) SI_UNIT ( .MILLI., .METRE. ) );
#5306=DIRECTION ( 'NONE',  ( 1.000000000000000000, 0.000000000000000000, 0.000000000000000000 ) ) ;
#5338=FILL_AREA_STYLE_COLOUR ( '', #19135 ) ;
#5461=PRESENTATION_STYLE_ASSIGNMENT (( #12618 ) ) ;
#5581=MANIFOLD_SOLID_BREP ( 'Chamfer1', #4672 ) ;
#5665=PRODUCT_CONTEXT ( 'NONE', #14753, 'mechanical' ) ;
#5677=CARTESIAN_POINT ( 'NONE',  ( 2.792295943733760366E-14, 11.99999999999999645, 2.500000000000000888 ) ) ;
#5680=( NAMED_UNIT ( * ) SI_UNIT ( $, .STERADIAN. ) SOLID_ANGLE_UNIT ( ) );
#5682=CARTESIAN_POINT ( 'NONE',  ( 1.218648372641311897E-15, 59.74999999999991473, 4.500000000000020428 ) ) ;
#5739=PLANE ( 'NONE',  #14207 ) ;
#5764=DIRECTION ( 'NONE',  ( -3.070652698126927723E-17, -1.000000000000000000, 4.167305704548413124E-17 ) ) ;
#5980=CARTESIAN_POINT ( 'NONE',  ( 2.775557561562891351E-14, 11.99999999999999645, 6.938893903907228378E-15 ) ) ;
#6026=CARTESIAN_POINT ( 'NONE',  ( -3.097522238704186748E-14, 59.74999999999991473, -4.499999999999967137 ) ) ;
#6138=CIRCLE ( 'NONE', #23039, 4.499999999999988454 ) ;
#6258=FILL_AREA_STYLE_COLOUR ( '', #7993 ) ;
#6296=UNCERTAINTY_MEASURE_WITH_UNIT (LENGTH_MEASURE( 1.000000000000000082E-05 ), #21237, 'distance_accuracy_value', 'NONE');
#6593=FILL_AREA_STYLE_COLOUR ( '', #970 ) ;
#6735=COLOUR_RGB ( '', 0.08235294, 0.09019608, 0.10196078) ;
#6740=DIRECTION ( 'NONE',  ( -3.070652698126927723E-17, -1.000000000000000000, 4.167305704548413124E-17 ) ) ;
#6795=DIRECTION ( 'NONE',  ( 5.551115123125796261E-17, -2.869019762633796499E-16, -1.000000000000000000 ) ) ;
#6822=CARTESIAN_POINT ( 'NONE',  ( 0.000000000000000000, 0.000000000000000000, 0.000000000000000000 ) ) ;
#7035=VERTEX_POINT ( 'NONE', #12351 ) ;
#7057=ORIENTED_EDGE ( 'NONE', *, *, #5044, .T. ) ;
#7107=DIRECTION ( 'NONE',  ( 5.551115123125677932E-17, 0.000000000000000000, -1.000000000000000000 ) ) ;
#7136=STYLED_ITEM ( 'NONE', ( #5461 ), #1324 ) ;
#7314=ORIENTED_EDGE ( 'NONE', *, *, #3301, .T. ) ;
#7328=SURFACE_STYLE_USAGE ( .BOTH. , #12244 ) ;
#7352=AXIS2_PLACEMENT_3D ( 'NONE', #6822, #13766, #21424 ) ;
#7668=SURFACE_STYLE_USAGE ( .BOTH. , #495 ) ;
#7701=( GEOMETRIC_REPRESENTATION_CONTEXT ( 3 ) GLOBAL_UNCERTAINTY_ASSIGNED_CONTEXT ( ( #629 ) ) GLOBAL_UNIT_ASSIGNED_CONTEXT ( ( #16359, #4348, #5680 ) ) REPRESENTATION_CONTEXT ( 'NONE', 'WORKASPACE' ) );
#7740=AXIS2_PLACEMENT_3D ( 'NONE', #9379, #16527, #18088 ) ;
#7753=CARTESIAN_POINT ( 'NONE',  ( 2.789435349370705492E-14, 11.99999999999999645, -2.499999999999987121 ) ) ;
#7884=ORIENTED_EDGE ( 'NONE', *, *, #21708, .F. ) ;
#7931=MECHANICAL_DESIGN_GEOMETRIC_PRESENTATION_REPRESENTATION('',(#16559),#4550);
#7934=VERTEX_POINT ( 'NONE', #14761 ) ;
#7961=ADVANCED_FACE ( 'NONE', ( #1895 ), #1558, .F. ) ;
#7969=EDGE_CURVE ( 'NONE', #20156, #17539, #9375, .T. ) ;
#7986=CARTESIAN_POINT ( 'NONE',  ( 2.789435349370705492E-14, 11.99999999999999645, -2.499999999999987121 ) ) ;
#7993=COLOUR_RGB ( '', 0.08235294, 0.09019608, 0.10196078) ;
#8019=CONICAL_SURFACE ( 'NONE', #9902, 4.499999999999988454, 0.7853981633974396193 ) ;
#8124=EDGE_LOOP ( 'NONE', ( #12653, #7314 ) ) ;
#8130=CIRCLE ( 'NONE', #11129, 4.249999999999965361 ) ;
#8145=UNCERTAINTY_MEASURE_WITH_UNIT (LENGTH_MEASURE( 1.000000000000000082E-05 ), #10644, 'distance_accuracy_value', 'NONE');
#8150=CARTESIAN_POINT ( 'NONE',  ( 2.775557561562891351E-14, 11.99999999999999645, 6.938893903907228378E-15 ) ) ;
#8238=ORIENTED_EDGE ( 'NONE', *, *, #81, .T. ) ;
#8349=( NAMED_UNIT ( * ) SI_UNIT ( $, .STERADIAN. ) SOLID_ANGLE_UNIT ( ) );
#8433=CYLINDRICAL_SURFACE ( 'NONE', #18826, 2.499999999999993783 ) ;
#8540=DIRECTION ( 'NONE',  ( 5.551115123125677932E-17, 0.000000000000000000, -1.000000000000000000 ) ) ;
#8631=( NAMED_UNIT ( * ) PLANE_ANGLE_UNIT ( ) SI_UNIT ( $, .RADIAN. ) );
#8735=DIRECTION ( 'NONE',  ( 5.551115123125677932E-17, 0.000000000000000000, -1.000000000000000000 ) ) ;
#8890=( NAMED_UNIT ( * ) PLANE_ANGLE_UNIT ( ) SI_UNIT ( $, .RADIAN. ) );
#9097=UNCERTAINTY_MEASURE_WITH_UNIT (LENGTH_MEASURE( 1.000000000000000082E-05 ), #5214, 'distance_accuracy_value', 'NONE');
#9316=FILL_AREA_STYLE ('',( #18605 ) ) ;
#9375=CIRCLE ( 'NONE', #10493, 2.499999999999993783 ) ;
#9379=CARTESIAN_POINT ( 'NONE',  ( 0.000000000000000000, 0.000000000000000000, 0.000000000000000000 ) ) ;
#9464=DIRECTION ( 'NONE',  ( 5.551115123125733398E-17, 0.000000000000000000, -1.000000000000000000 ) ) ;
#9555=LINE ( 'NONE', #6026, #17321 ) ;
#9731=FACE_OUTER_BOUND ( 'NONE', #18841, .T. ) ;
#9902=AXIS2_PLACEMENT_3D ( 'NONE', #1222, #6740, #1560 ) ;
#9947=ORIENTED_EDGE ( 'NONE', *, *, #2109, .F. ) ;
#10300=FILL_AREA_STYLE_COLOUR ( '', #19213 ) ;
#10313=AXIS2_PLACEMENT_3D ( 'NONE', #8150, #15317, #18624 ) ;
#10480=MECHANICAL_DESIGN_GEOMETRIC_PRESENTATION_REPRESENTATION('',(#20634),#20652);
#10493=AXIS2_PLACEMENT_3D ( 'NONE', #12606, #18140, #7107 ) ;
#10532=FACE_OUTER_BOUND ( 'NONE', #15138, .T. ) ;
#10534=VECTOR ( 'NONE', #3775, 1000.000000000000000 ) ;
#10595=VERTEX_POINT ( 'NONE', #581 ) ;
#10644=( LENGTH_UNIT ( ) NAMED_UNIT ( * ) SI_UNIT ( .MILLI., .METRE. ) );
#10728=FILL_AREA_STYLE ('',( #16014 ) ) ;
#10831=VERTEX_POINT ( 'NONE', #23160 ) ;
#10840=CARTESIAN_POINT ( 'NONE',  ( 1.387778780781445676E-16, -7.172549406584475716E-16, -2.499999999999993783 ) ) ;
#10876=DIRECTION ( 'NONE',  ( 5.551115123125796261E-17, -2.869019762633797485E-16, -1.000000000000000000 ) ) ;
#10993=PRODUCT_DEFINITION_CONTEXT ( 'detailed design', #22003, 'design' ) ;
#11036=LINE ( 'NONE', #12804, #4738 ) ;
#11059=AXIS2_PLACEMENT_3D ( 'NONE', #21796, #3897, #16475 ) ;
#11095=( GEOMETRIC_REPRESENTATION_CONTEXT ( 3 ) GLOBAL_UNCERTAINTY_ASSIGNED_CONTEXT ( ( #17299 ) ) GLOBAL_UNIT_ASSIGNED_CONTEXT ( ( #5172, #19639, #8349 ) ) REPRESENTATION_CONTEXT ( 'NONE', 'WORKASPACE' ) );
#11129=AXIS2_PLACEMENT_3D ( 'NONE', #15469, #15698, #15932 ) ;
#11194=FILL_AREA_STYLE ('',( #6258 ) ) ;
#11354=DIRECTION ( 'NONE',  ( -5.551115123125796261E-17, 2.869019762633796499E-16, 1.000000000000000000 ) ) ;
#11476=DIRECTION ( 'NONE',  ( 3.070652698126929572E-17, 1.000000000000000000, -2.869019762633796499E-16 ) ) ;
#11624=CARTESIAN_POINT ( 'NONE',  ( 0.000000000000000000, 0.000000000000000000, 0.000000000000000000 ) ) ;
#11650=SHAPE_REPRESENTATION ( 'Rod', ( #22115 ), #19511 ) ;
#11669=ADVANCED_FACE ( 'NONE', ( #19206 ), #8019, .T. ) ;
#11844=ORIENTED_EDGE ( 'NONE', *, *, #5044, .F. ) ;
#11903=DIRECTION ( 'NONE',  ( -3.070652698126927723E-17, -1.000000000000000000, 4.167305704548413124E-17 ) ) ;
#12150=( NAMED_UNIT ( * ) SI_UNIT ( $, .STERADIAN. ) SOLID_ANGLE_UNIT ( ) );
#12244=SURFACE_SIDE_STYLE ('',( #159 ) ) ;
#12334=FACE_OUTER_BOUND ( 'NONE', #21066, .T. ) ;
#12351=CARTESIAN_POINT ( 'NONE',  ( 1.218648372641069717E-15, 1.875287567046784119E-16, 4.500000000000000000 ) ) ;
#12483=CARTESIAN_POINT ( 'NONE',  ( 2.775557561562891351E-14, 11.99999999999999645, 6.938893903907228378E-15 ) ) ;
#12521=CARTESIAN_POINT ( 'NONE',  ( 2.775557561562891351E-14, 11.99999999999999645, 6.938893903907228378E-15 ) ) ;
#12577=MECHANICAL_DESIGN_GEOMETRIC_PRESENTATION_REPRESENTATION('',(#4302),#7701);
#12606=CARTESIAN_POINT ( 'NONE',  ( 2.775557561562891351E-14, 11.99999999999999645, 6.938893903907228378E-15 ) ) ;
#12618=SURFACE_STYLE_USAGE ( .BOTH. , #21583 ) ;
#12625=CIRCLE ( 'NONE', #7740, 4.499999999999988454 ) ;
#12653=ORIENTED_EDGE ( 'NONE', *, *, #4894, .T. ) ;
#12680=VERTEX_POINT ( 'NONE', #1465 ) ;
#12804=CARTESIAN_POINT ( 'NONE',  ( -3.092373168850688607E-14, 59.74999999999991473, 4.500000000000008882 ) ) ;
#12890=ORIENTED_EDGE ( 'NONE', *, *, #913, .T. ) ;
#12966=DIRECTION ( 'NONE',  ( 1.753951801195068057E-17, -0.7071067811865545671, -0.7071067811865404673 ) ) ;
#13152=DIRECTION ( 'NONE',  ( -3.070652698126929572E-17, -1.000000000000000000, 2.869019762633796499E-16 ) ) ;
#13195=DIRECTION ( 'NONE',  ( -3.070652698126927723E-17, -1.000000000000000000, 4.167305704548413124E-17 ) ) ;
#13210=ORIENTED_EDGE ( 'NONE', *, *, #7969, .T. ) ;
#13228=ORIENTED_EDGE ( 'NONE', *, *, #3301, .F. ) ;
#13325=CIRCLE ( 'NONE', #21961, 2.499999999999993783 ) ;
#13431=PRESENTATION_STYLE_ASSIGNMENT (( #16582 ) ) ;
#13566=LINE ( 'NONE', #16849, #21799 ) ;
#13679=CONICAL_SURFACE ( 'NONE', #928, 4.499999999999988454, 0.7853981633974396193 ) ;
#13766=DIRECTION ( 'NONE',  ( -3.070652698126927723E-17, -1.000000000000000000, 4.167305704548413124E-17 ) ) ;
#13892=EDGE_CURVE ( 'NONE', #15346, #7035, #13566, .T. ) ;
#13901=ORIENTED_EDGE ( 'NONE', *, *, #16785, .F. ) ;
#13938=LINE ( 'NONE', #7986, #21196 ) ;
#14033=DIRECTION ( 'NONE',  ( -3.070652698126927723E-17, -1.000000000000000000, 4.167305704548413124E-17 ) ) ;
#14068=SURFACE_STYLE_FILL_AREA ( #14184 ) ;
#14086=PLANE ( 'NONE',  #22253 ) ;
#14153=EDGE_CURVE ( 'NONE', #17539, #12680, #380, .T. ) ;
#14184=FILL_AREA_STYLE ('',( #10300 ) ) ;
#14207=AXIS2_PLACEMENT_3D ( 'NONE', #22196, #11476, #11354 ) ;
#14301=( NAMED_UNIT ( * ) SI_UNIT ( $, .STERADIAN. ) SOLID_ANGLE_UNIT ( ) );
#14481=SHAPE_DEFINITION_REPRESENTATION ( #19064, #11650 ) ;
#14495=( NAMED_UNIT ( * ) SI_UNIT ( $, .STERADIAN. ) SOLID_ANGLE_UNIT ( ) );
#14547=AXIS2_PLACEMENT_3D ( 'NONE', #5980, #13152, #4185 ) ;
#14609=CYLINDRICAL_SURFACE ( 'NONE', #11059, 4.499999999999988454 ) ;
#14753=APPLICATION_CONTEXT ( 'automotive_design' ) ;
#14761=CARTESIAN_POINT ( 'NONE',  ( -3.092826256371965993E-14, 60.00000000000000000, 4.249999999999983125 ) ) ;
#14772=EDGE_LOOP ( 'NONE', ( #22764, #9947 ) ) ;
#14806=DIRECTION ( 'NONE',  ( 5.551115123125796261E-17, -2.869019762633797485E-16, -1.000000000000000000 ) ) ;
#15058=( NAMED_UNIT ( * ) SI_UNIT ( $, .STERADIAN. ) SOLID_ANGLE_UNIT ( ) );
#15138=EDGE_LOOP ( 'NONE', ( #3911, #2849, #21808, #16696 ) ) ;
#15154=DIRECTION ( 'NONE',  ( -3.070652698126927723E-17, -1.000000000000000000, 4.167305704548413124E-17 ) ) ;
#15317=DIRECTION ( 'NONE',  ( -3.070652698126927723E-17, -1.000000000000000000, 4.167305704548413124E-17 ) ) ;
#15346=VERTEX_POINT ( 'NONE', #5682 ) ;
#15469=CARTESIAN_POINT ( 'NONE',  ( -2.428612866367529932E-14, 60.00000000000000000, 6.938893903907228378E-15 ) ) ;
#15544=ORIENTED_EDGE ( 'NONE', *, *, #20753, .T. ) ;
#15545=ORIENTED_EDGE ( 'NONE', *, *, #2109, .T. ) ;
#15698=DIRECTION ( 'NONE',  ( 3.070652698126927723E-17, 1.000000000000000000, -4.167305704548413124E-17 ) ) ;
#15856=CYLINDRICAL_SURFACE ( 'NONE', #7352, 4.499999999999988454 ) ;
#15932=DIRECTION ( 'NONE',  ( -5.551115123125796261E-17, 0.000000000000000000, 1.000000000000000000 ) ) ;
#15997=ADVANCED_FACE ( 'NONE', ( #22921, #21154 ), #14086, .T. ) ;
#16014=FILL_AREA_STYLE_COLOUR ( '', #6735 ) ;
#16359=( LENGTH_UNIT ( ) NAMED_UNIT ( * ) SI_UNIT ( .MILLI., .METRE. ) );
#16475=DIRECTION ( 'NONE',  ( 5.551115123125797493E-17, -2.869019762633797485E-16, -1.000000000000000000 ) ) ;
#16527=DIRECTION ( 'NONE',  ( -3.070652698126927723E-17, -1.000000000000000000, 4.167305704548413124E-17 ) ) ;
#16556=DIRECTION ( 'NONE',  ( -3.070652698126927723E-17, -1.000000000000000000, 4.167305704548413124E-17 ) ) ;
#16559=STYLED_ITEM ( 'NONE', ( #3255 ), #20730 ) ;
#16582=SURFACE_STYLE_USAGE ( .BOTH. , #2599 ) ;
#16592=SHAPE_REPRESENTATION_RELATIONSHIP ( 'NONE' , 'NONE' ,  #11650, #1324 ) ;
#16696=ORIENTED_EDGE ( 'NONE', *, *, #19433, .T. ) ;
#16785=EDGE_CURVE ( 'NONE', #235, #10831, #4962, .T. ) ;
#16812=SURFACE_STYLE_FILL_AREA ( #9316 ) ;
#16816=DIRECTION ( 'NONE',  ( -5.551115123125733398E-17, 0.000000000000000000, 1.000000000000000000 ) ) ;
#16849=CARTESIAN_POINT ( 'NONE',  ( 3.012908790756472548E-16, 1.291058893185205491E-15, 4.499999999999988454 ) ) ;
#16870=MECHANICAL_DESIGN_GEOMETRIC_PRESENTATION_REPRESENTATION('',(#7136),#4100);
#16974=EDGE_CURVE ( 'NONE', #235, #15346, #6138, .T. ) ;
#16986=( GEOMETRIC_REPRESENTATION_CONTEXT ( 3 ) GLOBAL_UNCERTAINTY_ASSIGNED_CONTEXT ( ( #22029 ) ) GLOBAL_UNIT_ASSIGNED_CONTEXT ( ( #18484, #18260, #15058 ) ) REPRESENTATION_CONTEXT ( 'NONE', 'WORKASPACE' ) );
#17092=ORIENTED_EDGE ( 'NONE', *, *, #81, .F. ) ;
#17299=UNCERTAINTY_MEASURE_WITH_UNIT (LENGTH_MEASURE( 1.000000000000000082E-05 ), #5172, 'distance_accuracy_value', 'NONE');
#17321=VECTOR ( 'NONE', #12966, 1000.000000000000000 ) ;
#17365=STYLED_ITEM ( 'NONE', ( #13431 ), #5581 ) ;
#17474=CARTESIAN_POINT ( 'NONE',  ( -2.428612866367529932E-14, 60.00000000000000000, 6.938893903907228378E-15 ) ) ;
#17513=SURFACE_SIDE_STYLE ('',( #19397 ) ) ;
#17539=VERTEX_POINT ( 'NONE', #22895 ) ;
#17541=CARTESIAN_POINT ( 'NONE',  ( 1.167157674106084754E-15, 59.74999999999991473, -4.499999999999978684 ) ) ;
#17567=EDGE_CURVE ( 'NONE', #20156, #1550, #13938, .T. ) ;
#17628=ORIENTED_EDGE ( 'NONE', *, *, #14153, .T. ) ;
#17812=( LENGTH_UNIT ( ) NAMED_UNIT ( * ) SI_UNIT ( .MILLI., .METRE. ) );
#17839=ORIENTED_EDGE ( 'NONE', *, *, #16974, .T. ) ;
#17874=ADVANCED_FACE ( 'NONE', ( #4044 ), #13679, .T. ) ;
#17929=EDGE_LOOP ( 'NONE', ( #11844, #12890, #19194, #20689 ) ) ;
#18088=DIRECTION ( 'NONE',  ( 5.551115123125797493E-17, -2.869019762633797485E-16, -1.000000000000000000 ) ) ;
#18140=DIRECTION ( 'NONE',  ( -3.070652698126927723E-17, -1.000000000000000000, 4.167305704548413124E-17 ) ) ;
#18218=FACE_OUTER_BOUND ( 'NONE', #18969, .T. ) ;
#18260=( NAMED_UNIT ( * ) PLANE_ANGLE_UNIT ( ) SI_UNIT ( $, .RADIAN. ) );
#18380=SURFACE_STYLE_FILL_AREA ( #11194 ) ;
#18404=DIRECTION ( 'NONE',  ( -3.070652698126927723E-17, -1.000000000000000000, 4.167305704548413124E-17 ) ) ;
#18484=( LENGTH_UNIT ( ) NAMED_UNIT ( * ) SI_UNIT ( .MILLI., .METRE. ) );
#18572=CARTESIAN_POINT ( 'NONE',  ( 0.000000000000000000, 0.000000000000000000, 0.000000000000000000 ) ) ;
#18605=FILL_AREA_STYLE_COLOUR ( '', #20078 ) ;
#18624=DIRECTION ( 'NONE',  ( 5.551115123125677932E-17, 0.000000000000000000, -1.000000000000000000 ) ) ;
#18738=ORIENTED_EDGE ( 'NONE', *, *, #13892, .F. ) ;
#18826=AXIS2_PLACEMENT_3D ( 'NONE', #12521, #1480, #8540 ) ;
#18841=EDGE_LOOP ( 'NONE', ( #808, #7057 ) ) ;
#18880=EDGE_LOOP ( 'NONE', ( #18738, #15544, #378, #13228 ) ) ;
#18949=EDGE_LOOP ( 'NONE', ( #17092, #17628, #15545, #2555 ) ) ;
#18969=EDGE_LOOP ( 'NONE', ( #13210, #8238 ) ) ;
#18982=CARTESIAN_POINT ( 'NONE',  ( 2.498001805406602216E-16, -1.291058893185205491E-15, -4.499999999999988454 ) ) ;
#18986=MECHANICAL_DESIGN_GEOMETRIC_PRESENTATION_REPRESENTATION('',(#23127),#11095);
#19064=PRODUCT_DEFINITION_SHAPE ( 'NONE', 'NONE',  #2001 ) ;
#19135=COLOUR_RGB ( '', 0.08235294, 0.09019608, 0.10196078) ;
#19194=ORIENTED_EDGE ( 'NONE', *, *, #16974, .F. ) ;
#19206=FACE_OUTER_BOUND ( 'NONE', #17929, .T. ) ;
#19213=COLOUR_RGB ( '', 0.09019608, 0.27058824, 0.51372549) ;
#19361=DIRECTION ( 'NONE',  ( 3.070652698126927723E-17, 1.000000000000000000, -4.167305704548413124E-17 ) ) ;
#19397=SURFACE_STYLE_FILL_AREA ( #5057 ) ;
#19398=AXIS2_PLACEMENT_3D ( 'NONE', #17474, #19361, #1484 ) ;
#19433=EDGE_CURVE ( 'NONE', #1550, #12680, #13325, .T. ) ;
#19511=( GEOMETRIC_REPRESENTATION_CONTEXT ( 3 ) GLOBAL_UNCERTAINTY_ASSIGNED_CONTEXT ( ( #22289 ) ) GLOBAL_UNIT_ASSIGNED_CONTEXT ( ( #17812, #8631, #12150 ) ) REPRESENTATION_CONTEXT ( 'NONE', 'WORKASPACE' ) );
#19515=AXIS2_PLACEMENT_3D ( 'NONE', #12483, #14033, #8735 ) ;
#19567=( NAMED_UNIT ( * ) PLANE_ANGLE_UNIT ( ) SI_UNIT ( $, .RADIAN. ) );
#19589=SURFACE_SIDE_STYLE ('',( #14068 ) ) ;
#19639=( NAMED_UNIT ( * ) PLANE_ANGLE_UNIT ( ) SI_UNIT ( $, .RADIAN. ) );
#19693=FILL_AREA_STYLE ('',( #5338 ) ) ;
#19781=CIRCLE ( 'NONE', #19398, 4.249999999999965361 ) ;
#19798=ADVANCED_FACE ( 'NONE', ( #20494 ), #14609, .T. ) ;
#19827=CARTESIAN_POINT ( 'NONE',  ( 0.000000000000000000, 0.000000000000000000, 0.000000000000000000 ) ) ;
#20017=DIRECTION ( 'NONE',  ( -3.070652698126927723E-17, -1.000000000000000000, 4.167305704548413124E-17 ) ) ;
#20036=( NAMED_UNIT ( * ) SI_UNIT ( $, .STERADIAN. ) SOLID_ANGLE_UNIT ( ) );
#20078=COLOUR_RGB ( '', 0.72549020, 0.75294118, 0.79215686) ;
#20156=VERTEX_POINT ( 'NONE', #7753 ) ;
#20204=CIRCLE ( 'NONE', #4789, 4.499999999999988454 ) ;
#20211=AXIS2_PLACEMENT_3D ( 'NONE', #18572, #5764, #14806 ) ;
#20469=CIRCLE ( 'NONE', #10313, 2.499999999999993783 ) ;
#20494=FACE_OUTER_BOUND ( 'NONE', #18880, .T. ) ;
#20634=STYLED_ITEM ( 'NONE', ( #3777 ), #7961 ) ;
#20652=( GEOMETRIC_REPRESENTATION_CONTEXT ( 3 ) GLOBAL_UNCERTAINTY_ASSIGNED_CONTEXT ( ( #9097 ) ) GLOBAL_UNIT_ASSIGNED_CONTEXT ( ( #5214, #21455, #14495 ) ) REPRESENTATION_CONTEXT ( 'NONE', 'WORKASPACE' ) );
#20689=ORIENTED_EDGE ( 'NONE', *, *, #20792, .F. ) ;
#20730=ADVANCED_FACE ( 'NONE', ( #10532 ), #8433, .F. ) ;
#20753=EDGE_CURVE ( 'NONE', #15346, #235, #21087, .T. ) ;
#20792=EDGE_CURVE ( 'NONE', #10595, #235, #9555, .T. ) ;
#20808=ORIENTED_EDGE ( 'NONE', *, *, #913, .F. ) ;
#21066=EDGE_LOOP ( 'NONE', ( #17839, #2497, #3663, #13901 ) ) ;
#21087=CIRCLE ( 'NONE', #803, 4.499999999999988454 ) ;
#21154=FACE_OUTER_BOUND ( 'NONE', #8124, .T. ) ;
#21196=VECTOR ( 'NONE', #15154, 1000.000000000000000 ) ;
#21237=( LENGTH_UNIT ( ) NAMED_UNIT ( * ) SI_UNIT ( .MILLI., .METRE. ) );
#21424=DIRECTION ( 'NONE',  ( 5.551115123125797493E-17, -2.869019762633797485E-16, -1.000000000000000000 ) ) ;
#21455=( NAMED_UNIT ( * ) PLANE_ANGLE_UNIT ( ) SI_UNIT ( $, .RADIAN. ) );
#21583=SURFACE_SIDE_STYLE ('',( #3576 ) ) ;
#21708=EDGE_CURVE ( 'NONE', #10595, #7934, #19781, .T. ) ;
#21796=CARTESIAN_POINT ( 'NONE',  ( 0.000000000000000000, 0.000000000000000000, 0.000000000000000000 ) ) ;
#21799=VECTOR ( 'NONE', #22162, 1000.000000000000000 ) ;
#21808=ORIENTED_EDGE ( 'NONE', *, *, #17567, .T. ) ;
#21900=DIRECTION ( 'NONE',  ( -7.160938508832258108E-15, 0.000000000000000000, 1.000000000000000000 ) ) ;
#21961=AXIS2_PLACEMENT_3D ( 'NONE', #19827, #3706, #10876 ) ;
#22003=APPLICATION_CONTEXT ( 'automotive_design' ) ;
#22029=UNCERTAINTY_MEASURE_WITH_UNIT (LENGTH_MEASURE( 1.000000000000000082E-05 ), #18484, 'distance_accuracy_value', 'NONE');
#22115=AXIS2_PLACEMENT_3D ( 'NONE', #4943, #2963, #5306 ) ;
#22162=DIRECTION ( 'NONE',  ( -3.070652698126927723E-17, -1.000000000000000000, 4.167305704548413124E-17 ) ) ;
#22168=CARTESIAN_POINT ( 'NONE',  ( -3.122502256758252770E-14, 59.74999999999991473, 2.081668171172168513E-14 ) ) ;
#22196=CARTESIAN_POINT ( 'NONE',  ( -2.428612866367529932E-14, 60.00000000000000000, 6.938893903907228378E-15 ) ) ;
#22247=PRESENTATION_STYLE_ASSIGNMENT (( #7668 ) ) ;
#22253=AXIS2_PLACEMENT_3D ( 'NONE', #3394, #22800, #6795 ) ;
#22289=UNCERTAINTY_MEASURE_WITH_UNIT (LENGTH_MEASURE( 1.000000000000000082E-05 ), #17812, 'distance_accuracy_value', 'NONE');
#22456=ADVANCED_FACE ( 'NONE', ( #18218 ), #2084, .T. ) ;
#22764=ORIENTED_EDGE ( 'NONE', *, *, #19433, .F. ) ;
#22800=DIRECTION ( 'NONE',  ( -3.070652698126929572E-17, -1.000000000000000000, 2.869019762633796499E-16 ) ) ;
#22895=CARTESIAN_POINT ( 'NONE',  ( 2.773872027544998636E-14, 11.99999999999999645, 2.500000000000007105 ) ) ;
#22921=FACE_BOUND ( 'NONE', #14772, .T. ) ;
#23039=AXIS2_PLACEMENT_3D ( 'NONE', #4120, #20017, #21900 ) ;
#23127=STYLED_ITEM ( 'NONE', ( #3532 ), #492 ) ;
#23160=CARTESIAN_POINT ( 'NONE',  ( 2.498001805406602216E-16, -1.291058893185205491E-15, -4.499999999999988454 ) ) ;
ENDSEC;
END-ISO-10303-21;
